ISO-10303-21;
HEADER;
/* Generated by software containing ST-Developer
 * from STEP Tools, Inc. (www.steptools.com) 
 */

FILE_DESCRIPTION(
/* description */ (''),
/* implementation_level */ '2;1');

FILE_NAME(
/* name */ 'M3_Nut_03 (1).step',
/* time_stamp */ '2026-10-22T15:07:41+06:00',
/* author */ (''),
/* organization */ (''),
/* preprocessor_version */ 'ST-DEVELOPER v20.2',
/* originating_system */ 'Autodesk Translation Framework v15.15.0.0',
/* authorisation */ '');

FILE_SCHEMA (('AUTOMOTIVE_DESIGN { 1 0 10303 214 3 1 1 }'));
ENDSEC;

DATA;
#10=MECHANICAL_DESIGN_GEOMETRIC_PRESENTATION_REPRESENTATION('',(#2889),#19220);
#78=SHAPE_REPRESENTATION_RELATIONSHIP('SRR','None',#19281,#92);
#92=ADVANCED_BREP_SHAPE_REPRESENTATION('',(#106),#19217);
#106=MANIFOLD_SOLID_BREP('M3_Nut_03',#11325);
#620=FACE_BOUND('',#4443,.T.);
#621=FACE_BOUND('',#4445,.T.);
#797=PLANE('',#12619);
#798=PLANE('',#12620);
#799=PLANE('',#12621);
#800=PLANE('',#12622);
#801=PLANE('',#12623);
#802=PLANE('',#12624);
#803=PLANE('',#12625);
#804=PLANE('',#12626);
#1568=LINE('',#18847,#2423);
#1569=LINE('',#18852,#2424);
#1570=LINE('',#18854,#2425);
#1571=LINE('',#18856,#2426);
#1572=LINE('',#18857,#2427);
#1573=LINE('',#18860,#2428);
#1574=LINE('',#18862,#2429);
#1575=LINE('',#18863,#2430);
#1576=LINE('',#18866,#2431);
#1577=LINE('',#18868,#2432);
#1578=LINE('',#18869,#2433);
#1579=LINE('',#18872,#2434);
#1580=LINE('',#18874,#2435);
#1581=LINE('',#18875,#2436);
#1582=LINE('',#18878,#2437);
#1583=LINE('',#18880,#2438);
#1584=LINE('',#18881,#2439);
#1585=LINE('',#18883,#2440);
#1586=LINE('',#18884,#2441);
#2423=VECTOR('',#15727,1.49999999999999);
#2424=VECTOR('',#15732,10.);
#2425=VECTOR('',#15733,10.);
#2426=VECTOR('',#15734,10.);
#2427=VECTOR('',#15735,10.);
#2428=VECTOR('',#15738,10.);
#2429=VECTOR('',#15739,10.);
#2430=VECTOR('',#15740,10.);
#2431=VECTOR('',#15743,10.);
#2432=VECTOR('',#15744,10.);
#2433=VECTOR('',#15745,10.);
#2434=VECTOR('',#15748,10.);
#2435=VECTOR('',#15749,10.);
#2436=VECTOR('',#15750,10.);
#2437=VECTOR('',#15753,10.);
#2438=VECTOR('',#15754,10.);
#2439=VECTOR('',#15755,10.);
#2440=VECTOR('',#15758,10.);
#2441=VECTOR('',#15759,10.);
#2858=CYLINDRICAL_SURFACE('',#12616,1.465);
#2889=STYLED_ITEM('',(#19410),#106);
#3378=FACE_OUTER_BOUND('',#4435,.T.);
#3379=FACE_OUTER_BOUND('',#4436,.T.);
#3380=FACE_OUTER_BOUND('',#4437,.T.);
#3381=FACE_OUTER_BOUND('',#4438,.T.);
#3382=FACE_OUTER_BOUND('',#4439,.T.);
#3383=FACE_OUTER_BOUND('',#4440,.T.);
#3384=FACE_OUTER_BOUND('',#4441,.T.);
#3385=FACE_OUTER_BOUND('',#4442,.T.);
#3386=FACE_OUTER_BOUND('',#4444,.T.);
#4435=EDGE_LOOP('',(#10438,#10439,#10440,#10441));
#4436=EDGE_LOOP('',(#10442,#10443,#10444,#10445));
#4437=EDGE_LOOP('',(#10446,#10447,#10448,#10449));
#4438=EDGE_LOOP('',(#10450,#10451,#10452,#10453));
#4439=EDGE_LOOP('',(#10454,#10455,#10456,#10457));
#4440=EDGE_LOOP('',(#10458,#10459,#10460,#10461));
#4441=EDGE_LOOP('',(#10462,#10463,#10464,#10465));
#4442=EDGE_LOOP('',(#10466,#10467,#10468,#10469,#10470,#10471));
#4443=EDGE_LOOP('',(#10472));
#4444=EDGE_LOOP('',(#10473,#10474,#10475,#10476,#10477,#10478));
#4445=EDGE_LOOP('',(#10479));
#5135=CIRCLE('',#12617,1.465);
#5136=CIRCLE('',#12618,1.465);
#6079=VERTEX_POINT('',#18844);
#6080=VERTEX_POINT('',#18846);
#6081=VERTEX_POINT('',#18850);
#6082=VERTEX_POINT('',#18851);
#6083=VERTEX_POINT('',#18853);
#6084=VERTEX_POINT('',#18855);
#6085=VERTEX_POINT('',#18859);
#6086=VERTEX_POINT('',#18861);
#6087=VERTEX_POINT('',#18865);
#6088=VERTEX_POINT('',#18867);
#6089=VERTEX_POINT('',#18871);
#6090=VERTEX_POINT('',#18873);
#6091=VERTEX_POINT('',#18877);
#6092=VERTEX_POINT('',#18879);
#7550=EDGE_CURVE('',#6079,#6079,#5135,.T.);
#7551=EDGE_CURVE('',#6079,#6080,#1568,.T.);
#7552=EDGE_CURVE('',#6080,#6080,#5136,.F.);
#7553=EDGE_CURVE('',#6081,#6082,#1569,.T.);
#7554=EDGE_CURVE('',#6081,#6083,#1570,.T.);
#7555=EDGE_CURVE('',#6084,#6083,#1571,.T.);
#7556=EDGE_CURVE('',#6082,#6084,#1572,.T.);
#7557=EDGE_CURVE('',#6082,#6085,#1573,.T.);
#7558=EDGE_CURVE('',#6086,#6084,#1574,.T.);
#7559=EDGE_CURVE('',#6085,#6086,#1575,.T.);
#7560=EDGE_CURVE('',#6085,#6087,#1576,.T.);
#7561=EDGE_CURVE('',#6088,#6086,#1577,.T.);
#7562=EDGE_CURVE('',#6087,#6088,#1578,.T.);
#7563=EDGE_CURVE('',#6087,#6089,#1579,.T.);
#7564=EDGE_CURVE('',#6090,#6088,#1580,.T.);
#7565=EDGE_CURVE('',#6089,#6090,#1581,.T.);
#7566=EDGE_CURVE('',#6089,#6091,#1582,.T.);
#7567=EDGE_CURVE('',#6092,#6090,#1583,.T.);
#7568=EDGE_CURVE('',#6091,#6092,#1584,.T.);
#7569=EDGE_CURVE('',#6091,#6081,#1585,.T.);
#7570=EDGE_CURVE('',#6083,#6092,#1586,.T.);
#10438=ORIENTED_EDGE('',*,*,#7550,.F.);
#10439=ORIENTED_EDGE('',*,*,#7551,.T.);
#10440=ORIENTED_EDGE('',*,*,#7552,.F.);
#10441=ORIENTED_EDGE('',*,*,#7551,.F.);
#10442=ORIENTED_EDGE('',*,*,#7553,.F.);
#10443=ORIENTED_EDGE('',*,*,#7554,.T.);
#10444=ORIENTED_EDGE('',*,*,#7555,.F.);
#10445=ORIENTED_EDGE('',*,*,#7556,.F.);
#10446=ORIENTED_EDGE('',*,*,#7557,.F.);
#10447=ORIENTED_EDGE('',*,*,#7556,.T.);
#10448=ORIENTED_EDGE('',*,*,#7558,.F.);
#10449=ORIENTED_EDGE('',*,*,#7559,.F.);
#10450=ORIENTED_EDGE('',*,*,#7560,.F.);
#10451=ORIENTED_EDGE('',*,*,#7559,.T.);
#10452=ORIENTED_EDGE('',*,*,#7561,.F.);
#10453=ORIENTED_EDGE('',*,*,#7562,.F.);
#10454=ORIENTED_EDGE('',*,*,#7563,.F.);
#10455=ORIENTED_EDGE('',*,*,#7562,.T.);
#10456=ORIENTED_EDGE('',*,*,#7564,.F.);
#10457=ORIENTED_EDGE('',*,*,#7565,.F.);
#10458=ORIENTED_EDGE('',*,*,#7566,.F.);
#10459=ORIENTED_EDGE('',*,*,#7565,.T.);
#10460=ORIENTED_EDGE('',*,*,#7567,.F.);
#10461=ORIENTED_EDGE('',*,*,#7568,.F.);
#10462=ORIENTED_EDGE('',*,*,#7569,.F.);
#10463=ORIENTED_EDGE('',*,*,#7568,.T.);
#10464=ORIENTED_EDGE('',*,*,#7570,.F.);
#10465=ORIENTED_EDGE('',*,*,#7554,.F.);
#10466=ORIENTED_EDGE('',*,*,#7569,.T.);
#10467=ORIENTED_EDGE('',*,*,#7553,.T.);
#10468=ORIENTED_EDGE('',*,*,#7557,.T.);
#10469=ORIENTED_EDGE('',*,*,#7560,.T.);
#10470=ORIENTED_EDGE('',*,*,#7563,.T.);
#10471=ORIENTED_EDGE('',*,*,#7566,.T.);
#10472=ORIENTED_EDGE('',*,*,#7552,.T.);
#10473=ORIENTED_EDGE('',*,*,#7570,.T.);
#10474=ORIENTED_EDGE('',*,*,#7567,.T.);
#10475=ORIENTED_EDGE('',*,*,#7564,.T.);
#10476=ORIENTED_EDGE('',*,*,#7561,.T.);
#10477=ORIENTED_EDGE('',*,*,#7558,.T.);
#10478=ORIENTED_EDGE('',*,*,#7555,.T.);
#10479=ORIENTED_EDGE('',*,*,#7550,.T.);
#11254=ADVANCED_FACE('',(#3378),#2858,.F.);
#11255=ADVANCED_FACE('',(#3379),#797,.T.);
#11256=ADVANCED_FACE('',(#3380),#798,.T.);
#11257=ADVANCED_FACE('',(#3381),#799,.T.);
#11258=ADVANCED_FACE('',(#3382),#800,.T.);
#11259=ADVANCED_FACE('',(#3383),#801,.T.);
#11260=ADVANCED_FACE('',(#3384),#802,.T.);
#11261=ADVANCED_FACE('',(#3385,#620),#803,.T.);
#11262=ADVANCED_FACE('',(#3386,#621),#804,.F.);
#11325=CLOSED_SHELL('',(#11254,#11255,#11256,#11257,#11258,#11259,#11260,
#11261,#11262));
#12615=AXIS2_PLACEMENT_3D('',#18842,#15721,#15722);
#12616=AXIS2_PLACEMENT_3D('',#18843,#15723,#15724);
#12617=AXIS2_PLACEMENT_3D('',#18845,#15725,#15726);
#12618=AXIS2_PLACEMENT_3D('',#18848,#15728,#15729);
#12619=AXIS2_PLACEMENT_3D('',#18849,#15730,#15731);
#12620=AXIS2_PLACEMENT_3D('',#18858,#15736,#15737);
#12621=AXIS2_PLACEMENT_3D('',#18864,#15741,#15742);
#12622=AXIS2_PLACEMENT_3D('',#18870,#15746,#15747);
#12623=AXIS2_PLACEMENT_3D('',#18876,#15751,#15752);
#12624=AXIS2_PLACEMENT_3D('',#18882,#15756,#15757);
#12625=AXIS2_PLACEMENT_3D('',#18885,#15760,#15761);
#12626=AXIS2_PLACEMENT_3D('',#18886,#15762,#15763);
#15721=DIRECTION('axis',(0.,0.,1.));
#15722=DIRECTION('refdir',(1.,0.,0.));
#15723=DIRECTION('center_axis',(0.,-1.,0.));
#15724=DIRECTION('ref_axis',(-1.,0.,0.));
#15725=DIRECTION('center_axis',(0.,1.,0.));
#15726=DIRECTION('ref_axis',(-1.,0.,0.));
#15727=DIRECTION('',(0.,1.,0.));
#15728=DIRECTION('center_axis',(0.,1.,0.));
#15729=DIRECTION('ref_axis',(-1.,0.,0.));
#15730=DIRECTION('center_axis',(-0.866025403784439,0.,-0.499999999999999));
#15731=DIRECTION('ref_axis',(0.499999999999999,0.,-0.866025403784439));
#15732=DIRECTION('',(-0.499999999999999,0.,0.866025403784439));
#15733=DIRECTION('',(0.,-1.,0.));
#15734=DIRECTION('',(0.499999999999999,0.,-0.866025403784439));
#15735=DIRECTION('',(0.,-1.,0.));
#15736=DIRECTION('center_axis',(-0.866025403784439,0.,0.499999999999999));
#15737=DIRECTION('ref_axis',(-0.499999999999999,0.,-0.866025403784439));
#15738=DIRECTION('',(0.499999999999999,0.,0.866025403784439));
#15739=DIRECTION('',(-0.499999999999999,0.,-0.866025403784439));
#15740=DIRECTION('',(0.,-1.,0.));
#15741=DIRECTION('center_axis',(0.,0.,1.));
#15742=DIRECTION('ref_axis',(-1.,0.,0.));
#15743=DIRECTION('',(1.,0.,0.));
#15744=DIRECTION('',(-1.,0.,0.));
#15745=DIRECTION('',(0.,-1.,0.));
#15746=DIRECTION('center_axis',(0.866025403784438,0.,0.500000000000001));
#15747=DIRECTION('ref_axis',(-0.500000000000001,0.,0.866025403784438));
#15748=DIRECTION('',(0.500000000000001,0.,-0.866025403784438));
#15749=DIRECTION('',(-0.500000000000001,0.,0.866025403784438));
#15750=DIRECTION('',(0.,-1.,0.));
#15751=DIRECTION('center_axis',(0.866025403784439,0.,-0.5));
#15752=DIRECTION('ref_axis',(0.5,0.,0.866025403784439));
#15753=DIRECTION('',(-0.5,0.,-0.866025403784439));
#15754=DIRECTION('',(0.5,0.,0.866025403784439));
#15755=DIRECTION('',(0.,-1.,0.));
#15756=DIRECTION('center_axis',(4.61511044732058E-15,0.,-1.));
#15757=DIRECTION('ref_axis',(1.,0.,4.61511044732058E-15));
#15758=DIRECTION('',(-1.,0.,-4.61511044732058E-15));
#15759=DIRECTION('',(1.,0.,4.61511044732058E-15));
#15760=DIRECTION('center_axis',(0.,1.,0.));
#15761=DIRECTION('ref_axis',(-1.,0.,0.));
#15762=DIRECTION('center_axis',(0.,1.,0.));
#15763=DIRECTION('ref_axis',(-1.,0.,0.));
#18842=CARTESIAN_POINT('',(0.,0.,0.));
#18843=CARTESIAN_POINT('Origin',(67.9877341799264,58.5,25.7372649179816));
#18844=CARTESIAN_POINT('',(69.4527341799265,56.5,25.7372649179816));
#18845=CARTESIAN_POINT('Origin',(67.9877341799264,56.5,25.7372649179816));
#18846=CARTESIAN_POINT('',(69.4527341799265,58.5,25.7372649179816));
#18847=CARTESIAN_POINT('',(69.4527341799264,58.5,25.7372649179816));
#18848=CARTESIAN_POINT('Origin',(67.9877341799264,58.5,25.7372649179816));
#18849=CARTESIAN_POINT('Origin',(65.1009828339783,58.5,25.7372649179816));
#18850=CARTESIAN_POINT('',(66.5443585069524,58.5,23.2372649179816));
#18851=CARTESIAN_POINT('',(65.1009828339783,58.5,25.7372649179816));
#18852=CARTESIAN_POINT('',(66.5443585069524,58.5,23.2372649179816));
#18853=CARTESIAN_POINT('',(66.5443585069524,56.5,23.2372649179816));
#18854=CARTESIAN_POINT('',(66.5443585069524,58.5,23.2372649179816));
#18855=CARTESIAN_POINT('',(65.1009828339783,56.5,25.7372649179816));
#18856=CARTESIAN_POINT('',(66.5443585069524,56.5,23.2372649179816));
#18857=CARTESIAN_POINT('',(65.1009828339783,58.5,25.7372649179816));
#18858=CARTESIAN_POINT('Origin',(66.5443585069524,58.5,28.2372649179815));
#18859=CARTESIAN_POINT('',(66.5443585069524,58.5,28.2372649179815));
#18860=CARTESIAN_POINT('',(65.1009828339783,58.5,25.7372649179816));
#18861=CARTESIAN_POINT('',(66.5443585069524,56.5,28.2372649179815));
#18862=CARTESIAN_POINT('',(65.1009828339783,56.5,25.7372649179816));
#18863=CARTESIAN_POINT('',(66.5443585069524,58.5,28.2372649179815));
#18864=CARTESIAN_POINT('Origin',(69.4311098529005,58.5,28.2372649179815));
#18865=CARTESIAN_POINT('',(69.4311098529005,58.5,28.2372649179815));
#18866=CARTESIAN_POINT('',(66.5443585069524,58.5,28.2372649179815));
#18867=CARTESIAN_POINT('',(69.4311098529005,56.5,28.2372649179815));
#18868=CARTESIAN_POINT('',(66.5443585069524,56.5,28.2372649179815));
#18869=CARTESIAN_POINT('',(69.4311098529005,58.5,28.2372649179815));
#18870=CARTESIAN_POINT('Origin',(70.8744855258745,58.5,25.7372649179816));
#18871=CARTESIAN_POINT('',(70.8744855258745,58.5,25.7372649179816));
#18872=CARTESIAN_POINT('',(69.4311098529005,58.5,28.2372649179815));
#18873=CARTESIAN_POINT('',(70.8744855258745,56.5,25.7372649179816));
#18874=CARTESIAN_POINT('',(69.4311098529005,56.5,28.2372649179815));
#18875=CARTESIAN_POINT('',(70.8744855258745,58.5,25.7372649179816));
#18876=CARTESIAN_POINT('Origin',(69.4311098529005,58.5,23.2372649179816));
#18877=CARTESIAN_POINT('',(69.4311098529005,58.5,23.2372649179816));
#18878=CARTESIAN_POINT('',(70.8744855258745,58.5,25.7372649179816));
#18879=CARTESIAN_POINT('',(69.4311098529005,56.5,23.2372649179816));
#18880=CARTESIAN_POINT('',(70.8744855258745,56.5,25.7372649179816));
#18881=CARTESIAN_POINT('',(69.4311098529005,58.5,23.2372649179816));
#18882=CARTESIAN_POINT('Origin',(66.5443585069524,58.5,23.2372649179816));
#18883=CARTESIAN_POINT('',(69.4311098529005,58.5,23.2372649179816));
#18884=CARTESIAN_POINT('',(69.4311098529005,56.5,23.2372649179816));
#18885=CARTESIAN_POINT('Origin',(67.9877341799264,58.5,25.7372649179816));
#18886=CARTESIAN_POINT('Origin',(67.9877341799264,56.5,25.7372649179816));
#19201=UNCERTAINTY_MEASURE_WITH_UNIT(LENGTH_MEASURE(0.01),#19221,
'DISTANCE_ACCURACY_VALUE',
'Maximum model space distance between geometric entities at asserted c
onnectivities');
#19204=UNCERTAINTY_MEASURE_WITH_UNIT(LENGTH_MEASURE(0.01),#19221,
'DISTANCE_ACCURACY_VALUE',
'Maximum model space distance between geometric entities at asserted c
onnectivities');
#19217=(
GEOMETRIC_REPRESENTATION_CONTEXT(3)
GLOBAL_UNCERTAINTY_ASSIGNED_CONTEXT((#19201))
GLOBAL_UNIT_ASSIGNED_CONTEXT((#19221,#19223,#19224))
REPRESENTATION_CONTEXT('','3D')
);
#19220=(
GEOMETRIC_REPRESENTATION_CONTEXT(3)
GLOBAL_UNCERTAINTY_ASSIGNED_CONTEXT((#19204))
GLOBAL_UNIT_ASSIGNED_CONTEXT((#19221,#19223,#19224))
REPRESENTATION_CONTEXT('','3D')
);
#19221=(
LENGTH_UNIT()
NAMED_UNIT(*)
SI_UNIT(.MILLI.,.METRE.)
);
#19223=(
NAMED_UNIT(*)
PLANE_ANGLE_UNIT()
SI_UNIT($,.RADIAN.)
);
#19224=(
NAMED_UNIT(*)
SI_UNIT($,.STERADIAN.)
SOLID_ANGLE_UNIT()
);
#19237=SHAPE_DEFINITION_REPRESENTATION(#19252,#19281);
#19252=PRODUCT_DEFINITION_SHAPE('',$,#19297);
#19281=SHAPE_REPRESENTATION('',(#12615),#19217);
#19284=PRODUCT_DEFINITION_CONTEXT('part definition',#19331,'design');
#19297=PRODUCT_DEFINITION('M3_Nut_03 (1)','M3_Nut_03 (1)',#19312,#19284);
#19312=PRODUCT_DEFINITION_FORMATION('',$,#19345);
#19331=APPLICATION_CONTEXT(
'Core Data for Automotive Mechanical Design Process');
#19332=PRODUCT_CONTEXT('part definition',#19331,'mechanical');
#19345=PRODUCT('M3_Nut_03 (1)','M3_Nut_03 (1)',$,(#19332));
#19404=COLOUR_RGB('Black',0.12,0.14,0.17);
#19405=FILL_AREA_STYLE_COLOUR('',#19404);
#19406=FILL_AREA_STYLE('',(#19405));
#19407=SURFACE_STYLE_FILL_AREA(#19406);
#19408=SURFACE_SIDE_STYLE('',(#19407));
#19409=SURFACE_STYLE_USAGE(.BOTH.,#19408);
#19410=PRESENTATION_STYLE_ASSIGNMENT((#19409));
ENDSEC;
END-ISO-10303-21;
